ISO-10303-21;
HEADER;
/* Generated by software containing ST-Developer
 * from STEP Tools, Inc. (www.steptools.com) 
 */

FILE_DESCRIPTION(
/* description */ ('STEP AP203'),
/* implementation_level */ '2;1');

FILE_NAME(
/* name */ 'F02_M8_Crank_Retaining_Nut.step',
/* time_stamp */ '2026-11-15T15:04:01-08:00',
/* author */ (''),
/* organization */ (''),
/* preprocessor_version */ 'ST-DEVELOPER v20.2',
/* originating_system */ 'Autodesk Translation Framework v15.17.0.0',
/* authorisation */ '');

FILE_SCHEMA (('AUTOMOTIVE_DESIGN { 1 0 10303 214 3 1 1 }'));
ENDSEC;

DATA;
#10=MECHANICAL_DESIGN_GEOMETRIC_PRESENTATION_REPRESENTATION('',(#302),#16598);
#224=SHAPE_REPRESENTATION_RELATIONSHIP('SRR','None',#16718,#248);
#248=ADVANCED_BREP_SHAPE_REPRESENTATION('',(#272),#16594);
#272=MANIFOLD_SOLID_BREP('Body1',#9807);
#302=STYLED_ITEM('',(#16833),#272);
#422=FACE_BOUND('',#2088,.T.);
#423=FACE_BOUND('',#2090,.T.);
#874=PLANE('',#10829);
#875=PLANE('',#10830);
#876=PLANE('',#10831);
#877=PLANE('',#10832);
#878=PLANE('',#10833);
#879=PLANE('',#10834);
#880=PLANE('',#10835);
#881=PLANE('',#10836);
#1419=FACE_OUTER_BOUND('',#2086,.T.);
#1420=FACE_OUTER_BOUND('',#2087,.T.);
#1421=FACE_OUTER_BOUND('',#2089,.T.);
#1422=FACE_OUTER_BOUND('',#2091,.T.);
#1423=FACE_OUTER_BOUND('',#2092,.T.);
#1424=FACE_OUTER_BOUND('',#2093,.T.);
#1425=FACE_OUTER_BOUND('',#2094,.T.);
#1426=FACE_OUTER_BOUND('',#2095,.T.);
#1427=FACE_OUTER_BOUND('',#2096,.T.);
#2086=EDGE_LOOP('',(#8989,#8990,#8991,#8992));
#2087=EDGE_LOOP('',(#8993,#8994,#8995,#8996,#8997,#8998));
#2088=EDGE_LOOP('',(#8999));
#2089=EDGE_LOOP('',(#9000,#9001,#9002,#9003,#9004,#9005));
#2090=EDGE_LOOP('',(#9006));
#2091=EDGE_LOOP('',(#9007,#9008,#9009,#9010));
#2092=EDGE_LOOP('',(#9011,#9012,#9013,#9014));
#2093=EDGE_LOOP('',(#9015,#9016,#9017,#9018));
#2094=EDGE_LOOP('',(#9019,#9020,#9021,#9022));
#2095=EDGE_LOOP('',(#9023,#9024,#9025,#9026));
#2096=EDGE_LOOP('',(#9027,#9028,#9029,#9030));
#3106=LINE('',#16311,#4154);
#3107=LINE('',#16316,#4155);
#3108=LINE('',#16318,#4156);
#3109=LINE('',#16320,#4157);
#3110=LINE('',#16322,#4158);
#3111=LINE('',#16324,#4159);
#3112=LINE('',#16325,#4160);
#3113=LINE('',#16329,#4161);
#3114=LINE('',#16331,#4162);
#3115=LINE('',#16333,#4163);
#3116=LINE('',#16335,#4164);
#3117=LINE('',#16337,#4165);
#3118=LINE('',#16338,#4166);
#3119=LINE('',#16340,#4167);
#3120=LINE('',#16341,#4168);
#3121=LINE('',#16343,#4169);
#3122=LINE('',#16345,#4170);
#3123=LINE('',#16347,#4171);
#3124=LINE('',#16349,#4172);
#4154=VECTOR('',#13402,4.2);
#4155=VECTOR('',#13407,1000.);
#4156=VECTOR('',#13408,1000.);
#4157=VECTOR('',#13409,1000.);
#4158=VECTOR('',#13410,1000.);
#4159=VECTOR('',#13411,1000.);
#4160=VECTOR('',#13412,1000.);
#4161=VECTOR('',#13415,1000.);
#4162=VECTOR('',#13416,1000.);
#4163=VECTOR('',#13417,1000.);
#4164=VECTOR('',#13418,1000.);
#4165=VECTOR('',#13419,1000.);
#4166=VECTOR('',#13420,1000.);
#4167=VECTOR('',#13423,1000.);
#4168=VECTOR('',#13424,1000.);
#4169=VECTOR('',#13427,1000.);
#4170=VECTOR('',#13430,1000.);
#4171=VECTOR('',#13433,1000.);
#4172=VECTOR('',#13436,1000.);
#4443=CIRCLE('',#10827,4.2);
#4444=CIRCLE('',#10828,4.2);
#5251=VERTEX_POINT('',#16308);
#5252=VERTEX_POINT('',#16310);
#5253=VERTEX_POINT('',#16314);
#5254=VERTEX_POINT('',#16315);
#5255=VERTEX_POINT('',#16317);
#5256=VERTEX_POINT('',#16319);
#5257=VERTEX_POINT('',#16321);
#5258=VERTEX_POINT('',#16323);
#5259=VERTEX_POINT('',#16327);
#5260=VERTEX_POINT('',#16328);
#5261=VERTEX_POINT('',#16330);
#5262=VERTEX_POINT('',#16332);
#5263=VERTEX_POINT('',#16334);
#5264=VERTEX_POINT('',#16336);
#6507=EDGE_CURVE('',#5251,#5251,#4443,.T.);
#6508=EDGE_CURVE('',#5251,#5252,#3106,.T.);
#6509=EDGE_CURVE('',#5252,#5252,#4444,.T.);
#6510=EDGE_CURVE('',#5253,#5254,#3107,.T.);
#6511=EDGE_CURVE('',#5254,#5255,#3108,.T.);
#6512=EDGE_CURVE('',#5255,#5256,#3109,.T.);
#6513=EDGE_CURVE('',#5256,#5257,#3110,.T.);
#6514=EDGE_CURVE('',#5257,#5258,#3111,.T.);
#6515=EDGE_CURVE('',#5258,#5253,#3112,.T.);
#6516=EDGE_CURVE('',#5259,#5260,#3113,.T.);
#6517=EDGE_CURVE('',#5261,#5259,#3114,.T.);
#6518=EDGE_CURVE('',#5262,#5261,#3115,.T.);
#6519=EDGE_CURVE('',#5263,#5262,#3116,.T.);
#6520=EDGE_CURVE('',#5264,#5263,#3117,.T.);
#6521=EDGE_CURVE('',#5260,#5264,#3118,.T.);
#6522=EDGE_CURVE('',#5254,#5260,#3119,.T.);
#6523=EDGE_CURVE('',#5253,#5259,#3120,.T.);
#6524=EDGE_CURVE('',#5255,#5264,#3121,.T.);
#6525=EDGE_CURVE('',#5256,#5263,#3122,.T.);
#6526=EDGE_CURVE('',#5257,#5262,#3123,.T.);
#6527=EDGE_CURVE('',#5258,#5261,#3124,.T.);
#8989=ORIENTED_EDGE('',*,*,#6507,.T.);
#8990=ORIENTED_EDGE('',*,*,#6508,.T.);
#8991=ORIENTED_EDGE('',*,*,#6509,.F.);
#8992=ORIENTED_EDGE('',*,*,#6508,.F.);
#8993=ORIENTED_EDGE('',*,*,#6510,.T.);
#8994=ORIENTED_EDGE('',*,*,#6511,.T.);
#8995=ORIENTED_EDGE('',*,*,#6512,.T.);
#8996=ORIENTED_EDGE('',*,*,#6513,.T.);
#8997=ORIENTED_EDGE('',*,*,#6514,.T.);
#8998=ORIENTED_EDGE('',*,*,#6515,.T.);
#8999=ORIENTED_EDGE('',*,*,#6507,.F.);
#9000=ORIENTED_EDGE('',*,*,#6516,.F.);
#9001=ORIENTED_EDGE('',*,*,#6517,.F.);
#9002=ORIENTED_EDGE('',*,*,#6518,.F.);
#9003=ORIENTED_EDGE('',*,*,#6519,.F.);
#9004=ORIENTED_EDGE('',*,*,#6520,.F.);
#9005=ORIENTED_EDGE('',*,*,#6521,.F.);
#9006=ORIENTED_EDGE('',*,*,#6509,.T.);
#9007=ORIENTED_EDGE('',*,*,#6516,.T.);
#9008=ORIENTED_EDGE('',*,*,#6522,.F.);
#9009=ORIENTED_EDGE('',*,*,#6510,.F.);
#9010=ORIENTED_EDGE('',*,*,#6523,.T.);
#9011=ORIENTED_EDGE('',*,*,#6521,.T.);
#9012=ORIENTED_EDGE('',*,*,#6524,.F.);
#9013=ORIENTED_EDGE('',*,*,#6511,.F.);
#9014=ORIENTED_EDGE('',*,*,#6522,.T.);
#9015=ORIENTED_EDGE('',*,*,#6520,.T.);
#9016=ORIENTED_EDGE('',*,*,#6525,.F.);
#9017=ORIENTED_EDGE('',*,*,#6512,.F.);
#9018=ORIENTED_EDGE('',*,*,#6524,.T.);
#9019=ORIENTED_EDGE('',*,*,#6519,.T.);
#9020=ORIENTED_EDGE('',*,*,#6526,.F.);
#9021=ORIENTED_EDGE('',*,*,#6513,.F.);
#9022=ORIENTED_EDGE('',*,*,#6525,.T.);
#9023=ORIENTED_EDGE('',*,*,#6518,.T.);
#9024=ORIENTED_EDGE('',*,*,#6527,.F.);
#9025=ORIENTED_EDGE('',*,*,#6514,.F.);
#9026=ORIENTED_EDGE('',*,*,#6526,.T.);
#9027=ORIENTED_EDGE('',*,*,#6517,.T.);
#9028=ORIENTED_EDGE('',*,*,#6523,.F.);
#9029=ORIENTED_EDGE('',*,*,#6515,.F.);
#9030=ORIENTED_EDGE('',*,*,#6527,.T.);
#9230=CYLINDRICAL_SURFACE('',#10826,4.2);
#9744=ADVANCED_FACE('',(#1419),#9230,.F.);
#9745=ADVANCED_FACE('',(#1420,#422),#874,.T.);
#9746=ADVANCED_FACE('',(#1421,#423),#875,.F.);
#9747=ADVANCED_FACE('',(#1422),#876,.F.);
#9748=ADVANCED_FACE('',(#1423),#877,.F.);
#9749=ADVANCED_FACE('',(#1424),#878,.F.);
#9750=ADVANCED_FACE('',(#1425),#879,.F.);
#9751=ADVANCED_FACE('',(#1426),#880,.F.);
#9752=ADVANCED_FACE('',(#1427),#881,.F.);
#9807=CLOSED_SHELL('',(#9744,#9745,#9746,#9747,#9748,#9749,#9750,#9751,
#9752));
#10825=AXIS2_PLACEMENT_3D('',#16306,#13396,#13397);
#10826=AXIS2_PLACEMENT_3D('',#16307,#13398,#13399);
#10827=AXIS2_PLACEMENT_3D('',#16309,#13400,#13401);
#10828=AXIS2_PLACEMENT_3D('',#16312,#13403,#13404);
#10829=AXIS2_PLACEMENT_3D('',#16313,#13405,#13406);
#10830=AXIS2_PLACEMENT_3D('',#16326,#13413,#13414);
#10831=AXIS2_PLACEMENT_3D('',#16339,#13421,#13422);
#10832=AXIS2_PLACEMENT_3D('',#16342,#13425,#13426);
#10833=AXIS2_PLACEMENT_3D('',#16344,#13428,#13429);
#10834=AXIS2_PLACEMENT_3D('',#16346,#13431,#13432);
#10835=AXIS2_PLACEMENT_3D('',#16348,#13434,#13435);
#10836=AXIS2_PLACEMENT_3D('',#16350,#13437,#13438);
#13396=DIRECTION('axis',(0.,0.,1.));
#13397=DIRECTION('refdir',(1.,0.,0.));
#13398=DIRECTION('center_axis',(0.,0.,-1.));
#13399=DIRECTION('ref_axis',(-1.,0.,0.));
#13400=DIRECTION('center_axis',(0.,0.,1.));
#13401=DIRECTION('ref_axis',(1.,0.,0.));
#13402=DIRECTION('',(0.,0.,-1.));
#13403=DIRECTION('center_axis',(0.,0.,1.));
#13404=DIRECTION('ref_axis',(1.,0.,0.));
#13405=DIRECTION('center_axis',(0.,0.,1.));
#13406=DIRECTION('ref_axis',(1.,0.,0.));
#13407=DIRECTION('',(0.5,0.866025403784439,0.));
#13408=DIRECTION('',(-0.5,0.866025403784439,0.));
#13409=DIRECTION('',(-1.,1.1556266144132E-16,0.));
#13410=DIRECTION('',(-0.5,-0.866025403784438,0.));
#13411=DIRECTION('',(0.5,-0.866025403784439,0.));
#13412=DIRECTION('',(1.,-2.3112532288264E-16,0.));
#13413=DIRECTION('center_axis',(0.,0.,1.));
#13414=DIRECTION('ref_axis',(1.,0.,0.));
#13415=DIRECTION('',(0.5,0.866025403784439,0.));
#13416=DIRECTION('',(1.,-2.3112532288264E-16,0.));
#13417=DIRECTION('',(0.5,-0.866025403784439,0.));
#13418=DIRECTION('',(-0.5,-0.866025403784438,0.));
#13419=DIRECTION('',(-1.,1.1556266144132E-16,0.));
#13420=DIRECTION('',(-0.5,0.866025403784439,0.));
#13421=DIRECTION('center_axis',(-0.866025403784439,0.5,0.));
#13422=DIRECTION('ref_axis',(-0.5,-0.866025403784439,0.));
#13423=DIRECTION('',(0.,0.,-1.));
#13424=DIRECTION('',(0.,0.,-1.));
#13425=DIRECTION('center_axis',(-0.866025403784439,-0.5,0.));
#13426=DIRECTION('ref_axis',(0.5,-0.866025403784439,0.));
#13427=DIRECTION('',(0.,0.,-1.));
#13428=DIRECTION('center_axis',(-1.1556266144132E-16,-1.,0.));
#13429=DIRECTION('ref_axis',(1.,-1.1556266144132E-16,0.));
#13430=DIRECTION('',(0.,0.,-1.));
#13431=DIRECTION('center_axis',(0.866025403784439,-0.5,0.));
#13432=DIRECTION('ref_axis',(0.5,0.866025403784439,0.));
#13433=DIRECTION('',(0.,0.,-1.));
#13434=DIRECTION('center_axis',(0.866025403784439,0.5,0.));
#13435=DIRECTION('ref_axis',(-0.5,0.866025403784439,0.));
#13436=DIRECTION('',(0.,0.,-1.));
#13437=DIRECTION('center_axis',(2.3112532288264E-16,1.,0.));
#13438=DIRECTION('ref_axis',(-1.,2.3112532288264E-16,0.));
#16306=CARTESIAN_POINT('',(0.,0.,0.));
#16307=CARTESIAN_POINT('Origin',(0.,0.,6.));
#16308=CARTESIAN_POINT('',(4.2,-5.14351655641888E-16,6.));
#16309=CARTESIAN_POINT('Origin',(0.,0.,6.));
#16310=CARTESIAN_POINT('',(4.2,-5.14351655641888E-16,0.));
#16311=CARTESIAN_POINT('',(4.2,-5.14351655641888E-16,6.));
#16312=CARTESIAN_POINT('Origin',(0.,0.,0.));
#16313=CARTESIAN_POINT('Origin',(0.,0.,6.));
#16314=CARTESIAN_POINT('',(3.75277674973257,-6.5,6.));
#16315=CARTESIAN_POINT('',(7.50555349946513,0.,6.));
#16316=CARTESIAN_POINT('',(3.75277674973257,-6.5,6.));
#16317=CARTESIAN_POINT('',(3.75277674973257,6.5,6.));
#16318=CARTESIAN_POINT('',(7.50555349946513,0.,6.));
#16319=CARTESIAN_POINT('',(-3.75277674973257,6.5,6.));
#16320=CARTESIAN_POINT('',(3.75277674973257,6.5,6.));
#16321=CARTESIAN_POINT('',(-7.50555349946513,9.1916520689492E-16,6.));
#16322=CARTESIAN_POINT('',(-3.75277674973257,6.5,6.));
#16323=CARTESIAN_POINT('',(-3.75277674973257,-6.5,6.));
#16324=CARTESIAN_POINT('',(-7.50555349946513,9.1916520689492E-16,6.));
#16325=CARTESIAN_POINT('',(-3.75277674973257,-6.5,6.));
#16326=CARTESIAN_POINT('Origin',(0.,0.,0.));
#16327=CARTESIAN_POINT('',(3.75277674973257,-6.5,0.));
#16328=CARTESIAN_POINT('',(7.50555349946513,0.,0.));
#16329=CARTESIAN_POINT('',(3.75277674973257,-6.5,0.));
#16330=CARTESIAN_POINT('',(-3.75277674973257,-6.5,0.));
#16331=CARTESIAN_POINT('',(-3.75277674973257,-6.5,0.));
#16332=CARTESIAN_POINT('',(-7.50555349946513,9.1916520689492E-16,0.));
#16333=CARTESIAN_POINT('',(-7.50555349946513,9.1916520689492E-16,0.));
#16334=CARTESIAN_POINT('',(-3.75277674973257,6.5,0.));
#16335=CARTESIAN_POINT('',(-3.75277674973257,6.5,0.));
#16336=CARTESIAN_POINT('',(3.75277674973257,6.5,0.));
#16337=CARTESIAN_POINT('',(3.75277674973257,6.5,0.));
#16338=CARTESIAN_POINT('',(7.50555349946513,0.,0.));
#16339=CARTESIAN_POINT('Origin',(3.75277674973257,-6.5,6.));
#16340=CARTESIAN_POINT('',(7.50555349946513,0.,6.));
#16341=CARTESIAN_POINT('',(3.75277674973257,-6.5,6.));
#16342=CARTESIAN_POINT('Origin',(7.50555349946513,0.,6.));
#16343=CARTESIAN_POINT('',(3.75277674973257,6.5,6.));
#16344=CARTESIAN_POINT('Origin',(3.75277674973257,6.5,6.));
#16345=CARTESIAN_POINT('',(-3.75277674973257,6.5,6.));
#16346=CARTESIAN_POINT('Origin',(-3.75277674973257,6.5,6.));
#16347=CARTESIAN_POINT('',(-7.50555349946513,9.1916520689492E-16,6.));
#16348=CARTESIAN_POINT('Origin',(-7.50555349946513,9.1916520689492E-16,
6.));
#16349=CARTESIAN_POINT('',(-3.75277674973257,-6.5,6.));
#16350=CARTESIAN_POINT('Origin',(-3.75277674973257,-6.5,6.));
#16568=UNCERTAINTY_MEASURE_WITH_UNIT(LENGTH_MEASURE(0.01),#16599,
'DISTANCE_ACCURACY_VALUE',
'Maximum model space distance between geometric entities at asserted c
onnectivities');
#16572=UNCERTAINTY_MEASURE_WITH_UNIT(LENGTH_MEASURE(0.01),#16599,
'DISTANCE_ACCURACY_VALUE',
'Maximum model space distance between geometric entities at asserted c
onnectivities');
#16594=(
GEOMETRIC_REPRESENTATION_CONTEXT(3)
GLOBAL_UNCERTAINTY_ASSIGNED_CONTEXT((#16568))
GLOBAL_UNIT_ASSIGNED_CONTEXT((#16599,#16601,#16602))
REPRESENTATION_CONTEXT('','3D')
);
#16598=(
GEOMETRIC_REPRESENTATION_CONTEXT(3)
GLOBAL_UNCERTAINTY_ASSIGNED_CONTEXT((#16572))
GLOBAL_UNIT_ASSIGNED_CONTEXT((#16599,#16601,#16602))
REPRESENTATION_CONTEXT('','3D')
);
#16599=(
LENGTH_UNIT()
NAMED_UNIT(*)
SI_UNIT(.MILLI.,.METRE.)
);
#16601=(
NAMED_UNIT(*)
PLANE_ANGLE_UNIT()
SI_UNIT($,.RADIAN.)
);
#16602=(
NAMED_UNIT(*)
SI_UNIT($,.STERADIAN.)
SOLID_ANGLE_UNIT()
);
#16624=SHAPE_DEFINITION_REPRESENTATION(#16649,#16718);
#16649=PRODUCT_DEFINITION_SHAPE('',$,#16744);
#16718=SHAPE_REPRESENTATION('',(#10825),#16594);
#16722=PRODUCT_DEFINITION_CONTEXT('part definition',#16799,'design');
#16744=PRODUCT_DEFINITION('F02_M8_Crank_Retaining_Nut',
'F02_M8_Crank_Retaining_Nut',#16769,#16722);
#16769=PRODUCT_DEFINITION_FORMATION('',$,#16822);
#16799=APPLICATION_CONTEXT(
'Core Data for Automotive Mechanical Design Process');
#16800=PRODUCT_CONTEXT('part definition',#16799,'mechanical');
#16822=PRODUCT('F02_M8_Crank_Retaining_Nut',
'F02_M8_Crank_Retaining_Nut',$,(#16800));
#16833=PRESENTATION_STYLE_ASSIGNMENT((#16842));
#16842=SURFACE_STYLE_USAGE(.BOTH.,#16851);
#16851=SURFACE_SIDE_STYLE('',(#16860));
#16860=SURFACE_STYLE_FILL_AREA(#16869);
#16869=FILL_AREA_STYLE('Blue',(#16878));
#16878=FILL_AREA_STYLE_COLOUR('Blue',#16887);
#16887=COLOUR_RGB('Blue',0.,0.4,0.8);
ENDSEC;
END-ISO-10303-21;
